ISO-10303-21;
HEADER;
/* Generated by software containing ST-Developer
 * from STEP Tools, Inc. (www.steptools.com) 
 */
/* OPTION: using custom renumber hook */

FILE_DESCRIPTION(
/* description */ ('STEP AP242 Edition 2', 'CAx-IF Rec.Pracs.---Representation and Presentation of Product Manufa
cturing Information (PMI)---4.0---2014-10-13', 'CAx-IF Rec.Pracs.---3D Tessellated Geometry---0.4---2014-09-14', '2;1', 'CAx-IF Rec.Pracs.---User Defined Attributes---1.5---2016-08-15'),
/* implementation_level */ '2;1');

FILE_NAME(
/* name */ 'Part 1__PD10217.step',
/* time_stamp */ '2026-10-09T13:59:33Z',
/* author */ (''),
/* organization */ (''),
/* preprocessor_version */ 'ST-DEVELOPER v20',
/* originating_system */ 'ONSHAPE BY PTC INC, 1.221',
/* authorisation */ '  ');

FILE_SCHEMA (('AP242_MANAGED_MODEL_BASED_3D_ENGINEERING_MIM_LF { 1 0 10303 442 3 1 4 }'));
ENDSEC;

DATA;
#677=SHAPE_REPRESENTATION_RELATIONSHIP('','',#5695,#691);
#691=ADVANCED_BREP_SHAPE_REPRESENTATION('',(#5664),#10149);
#755=PLANE('',#6059);
#756=PLANE('',#6064);
#1524=ORIENTED_EDGE('',*,*,#2699,.F.);
#1525=ORIENTED_EDGE('',*,*,#2700,.F.);
#1526=ORIENTED_EDGE('',*,*,#2701,.F.);
#1527=ORIENTED_EDGE('',*,*,#2702,.T.);
#1528=ORIENTED_EDGE('',*,*,#2703,.T.);
#1529=ORIENTED_EDGE('',*,*,#2704,.T.);
#1530=ORIENTED_EDGE('',*,*,#2705,.T.);
#1531=ORIENTED_EDGE('',*,*,#2706,.F.);
#1532=ORIENTED_EDGE('',*,*,#2702,.F.);
#1533=ORIENTED_EDGE('',*,*,#2706,.T.);
#1534=ORIENTED_EDGE('',*,*,#2701,.T.);
#1535=ORIENTED_EDGE('',*,*,#2705,.F.);
#1536=ORIENTED_EDGE('',*,*,#2700,.T.);
#1537=ORIENTED_EDGE('',*,*,#2704,.F.);
#1538=ORIENTED_EDGE('',*,*,#2699,.T.);
#1539=ORIENTED_EDGE('',*,*,#2703,.F.);
#2699=EDGE_CURVE('',#3361,#3361,#3844,.T.);
#2700=EDGE_CURVE('',#3362,#3362,#3845,.T.);
#2701=EDGE_CURVE('',#3363,#3363,#3846,.T.);
#2702=EDGE_CURVE('',#3364,#3364,#3847,.T.);
#2703=EDGE_CURVE('',#3365,#3365,#3848,.T.);
#2704=EDGE_CURVE('',#3366,#3366,#3849,.T.);
#2705=EDGE_CURVE('',#3367,#3367,#3850,.T.);
#2706=EDGE_CURVE('',#3368,#3368,#3851,.T.);
#3361=VERTEX_POINT('',#9213);
#3362=VERTEX_POINT('',#9215);
#3363=VERTEX_POINT('',#9217);
#3364=VERTEX_POINT('',#9219);
#3365=VERTEX_POINT('',#9222);
#3366=VERTEX_POINT('',#9224);
#3367=VERTEX_POINT('',#9226);
#3368=VERTEX_POINT('',#9228);
#3844=CIRCLE('',#6060,0.00250000000000006);
#3845=CIRCLE('',#6061,0.0016601861613766);
#3846=CIRCLE('',#6062,0.00145132271222225);
#3847=CIRCLE('',#6063,0.059);
#3848=CIRCLE('',#6065,0.00250000000000006);
#3849=CIRCLE('',#6066,0.0016601861613766);
#3850=CIRCLE('',#6067,0.00145132271222225);
#3851=CIRCLE('',#6068,0.059);
#4326=EDGE_LOOP('',(#1524));
#4327=EDGE_LOOP('',(#1525));
#4328=EDGE_LOOP('',(#1526));
#4329=EDGE_LOOP('',(#1527));
#4330=EDGE_LOOP('',(#1528));
#4331=EDGE_LOOP('',(#1529));
#4332=EDGE_LOOP('',(#1530));
#4333=EDGE_LOOP('',(#1531));
#4334=EDGE_LOOP('',(#1532));
#4335=EDGE_LOOP('',(#1533));
#4336=EDGE_LOOP('',(#1534));
#4337=EDGE_LOOP('',(#1535));
#4338=EDGE_LOOP('',(#1536));
#4339=EDGE_LOOP('',(#1537));
#4340=EDGE_LOOP('',(#1538));
#4341=EDGE_LOOP('',(#1539));
#4774=FACE_BOUND('',#4326,.T.);
#4775=FACE_BOUND('',#4327,.T.);
#4776=FACE_BOUND('',#4328,.T.);
#4777=FACE_BOUND('',#4329,.T.);
#4778=FACE_BOUND('',#4330,.T.);
#4779=FACE_BOUND('',#4331,.T.);
#4780=FACE_BOUND('',#4332,.T.);
#4781=FACE_BOUND('',#4333,.T.);
#4782=FACE_BOUND('',#4334,.T.);
#4783=FACE_BOUND('',#4335,.T.);
#4784=FACE_BOUND('',#4336,.T.);
#4785=FACE_BOUND('',#4337,.T.);
#4786=FACE_BOUND('',#4338,.T.);
#4787=FACE_BOUND('',#4339,.T.);
#4788=FACE_BOUND('',#4340,.T.);
#4789=FACE_BOUND('',#4341,.T.);
#5092=CYLINDRICAL_SURFACE('',#6069,0.059);
#5093=CYLINDRICAL_SURFACE('',#6070,0.00145132271222225);
#5094=CYLINDRICAL_SURFACE('',#6071,0.0016601861613766);
#5095=CYLINDRICAL_SURFACE('',#6072,0.00250000000000006);
#5365=ADVANCED_FACE('',(#4774,#4775,#4776,#4777),#755,.T.);
#5366=ADVANCED_FACE('',(#4778,#4779,#4780,#4781),#756,.F.);
#5367=ADVANCED_FACE('',(#4782,#4783),#5092,.T.);
#5368=ADVANCED_FACE('',(#4784,#4785),#5093,.F.);
#5369=ADVANCED_FACE('',(#4786,#4787),#5094,.F.);
#5370=ADVANCED_FACE('',(#4788,#4789),#5095,.F.);
#5545=CLOSED_SHELL('',(#5365,#5366,#5367,#5368,#5369,#5370));
#5559=STYLED_ITEM('',(#5573),#5664);
#5573=PRESENTATION_STYLE_ASSIGNMENT((#5587));
#5587=SURFACE_STYLE_USAGE(.BOTH.,#5601);
#5601=SURFACE_SIDE_STYLE('',(#5615));
#5615=SURFACE_STYLE_FILL_AREA(#5629);
#5629=FILL_AREA_STYLE('',(#5643));
#5643=FILL_AREA_STYLE_COLOUR('',#5653);
#5653=COLOUR_RGB('', 0.40784314, 0.44705882, 0.49803922);
#5664=MANIFOLD_SOLID_BREP('Part 1',#5545);
#5679=SHAPE_DEFINITION_REPRESENTATION(#10192,#5695);
#5695=SHAPE_REPRESENTATION('Part 1',(#5704),#10149);
#5704=AXIS2_PLACEMENT_3D('',#8391,#6505,#6506);
#6059=AXIS2_PLACEMENT_3D('',#9211,#7364,#7365);
#6060=AXIS2_PLACEMENT_3D('',#9212,#7366,#7367);
#6061=AXIS2_PLACEMENT_3D('',#9214,#7368,#7369);
#6062=AXIS2_PLACEMENT_3D('',#9216,#7370,#7371);
#6063=AXIS2_PLACEMENT_3D('',#9218,#7372,#7373);
#6064=AXIS2_PLACEMENT_3D('',#9220,#7374,#7375);
#6065=AXIS2_PLACEMENT_3D('',#9221,#7376,#7377);
#6066=AXIS2_PLACEMENT_3D('',#9223,#7378,#7379);
#6067=AXIS2_PLACEMENT_3D('',#9225,#7380,#7381);
#6068=AXIS2_PLACEMENT_3D('',#9227,#7382,#7383);
#6069=AXIS2_PLACEMENT_3D('',#9229,#7384,#7385);
#6070=AXIS2_PLACEMENT_3D('',#9230,#7386,#7387);
#6071=AXIS2_PLACEMENT_3D('',#9231,#7388,#7389);
#6072=AXIS2_PLACEMENT_3D('',#9232,#7390,#7391);
#6505=DIRECTION('',(0.,0.,1.));
#6506=DIRECTION('',(1.,0.,0.));
#7364=DIRECTION('',(0.,1.,0.));
#7365=DIRECTION('',(0.,0.,1.));
#7366=DIRECTION('',(0.,1.,0.));
#7367=DIRECTION('',(-6.12323399573674E-17,0.,1.));
#7368=DIRECTION('',(0.,1.,0.));
#7369=DIRECTION('',(0.,0.,1.));
#7370=DIRECTION('',(0.,1.,0.));
#7371=DIRECTION('',(0.,0.,1.));
#7372=DIRECTION('',(0.,1.,0.));
#7373=DIRECTION('',(0.,0.,1.));
#7374=DIRECTION('',(0.,1.,0.));
#7375=DIRECTION('',(0.,0.,1.));
#7376=DIRECTION('',(0.,1.,0.));
#7377=DIRECTION('',(0.,0.,1.));
#7378=DIRECTION('',(0.,1.,0.));
#7379=DIRECTION('',(0.,0.,1.));
#7380=DIRECTION('',(0.,1.,0.));
#7381=DIRECTION('',(0.,0.,1.));
#7382=DIRECTION('',(0.,1.,0.));
#7383=DIRECTION('',(0.,0.,1.));
#7384=DIRECTION('',(0.,-1.,0.));
#7385=DIRECTION('',(0.,0.,-1.));
#7386=DIRECTION('',(0.,1.,0.));
#7387=DIRECTION('',(0.,0.,1.));
#7388=DIRECTION('',(0.,1.,0.));
#7389=DIRECTION('',(0.,0.,1.));
#7390=DIRECTION('',(0.,1.,0.));
#7391=DIRECTION('',(0.,0.,1.));
#8391=CARTESIAN_POINT('',(0.,0.,0.));
#9211=CARTESIAN_POINT('',(0.,0.0005,0.));
#9212=CARTESIAN_POINT('',(-2.76008920646131E-17,0.0005,5.55111512312578E-17));
#9213=CARTESIAN_POINT('',(-2.77539729145066E-17,0.0005,0.00250000000000011));
#9214=CARTESIAN_POINT('',(-0.00782575698925397,0.0005,-0.00322924205021303));
#9215=CARTESIAN_POINT('',(-0.00782575698925397,0.0005,-0.00156905588883643));
#9216=CARTESIAN_POINT('',(-0.0161768612294697,0.0005,-0.00667526484586793));
#9217=CARTESIAN_POINT('',(-0.0161768612294697,0.0005,-0.00522394213364568));
#9218=CARTESIAN_POINT('',(0.,0.0005,0.));
#9219=CARTESIAN_POINT('',(0.,0.0005,0.059));
#9220=CARTESIAN_POINT('',(0.,0.,0.));
#9221=CARTESIAN_POINT('',(-2.76008920646131E-17,0.,5.55111512312578E-17));
#9222=CARTESIAN_POINT('',(-2.76008920646131E-17,0.,0.00250000000000011));
#9223=CARTESIAN_POINT('',(-0.00782575698925397,0.,-0.00322924205021303));
#9224=CARTESIAN_POINT('',(-0.00782575698925397,0.,-0.00156905588883643));
#9225=CARTESIAN_POINT('',(-0.0161768612294697,0.,-0.00667526484586793));
#9226=CARTESIAN_POINT('',(-0.0161768612294697,0.,-0.00522394213364568));
#9227=CARTESIAN_POINT('',(0.,0.,0.));
#9228=CARTESIAN_POINT('',(0.,0.,0.059));
#9229=CARTESIAN_POINT('',(0.,0.0005,0.));
#9230=CARTESIAN_POINT('',(-0.0161768612294697,-0.0095,-0.00667526484586793));
#9231=CARTESIAN_POINT('',(-0.00782575698925397,-0.0095,-0.00322924205021303));
#9232=CARTESIAN_POINT('',(-2.76008920646131E-17,-0.0245,5.55111512312578E-17));
#10141=MECHANICAL_DESIGN_GEOMETRIC_PRESENTATION_REPRESENTATION('',(#5559),#10142);
#10142=(
GEOMETRIC_REPRESENTATION_CONTEXT(3)
GLOBAL_UNCERTAINTY_ASSIGNED_CONTEXT((#10158))
GLOBAL_UNIT_ASSIGNED_CONTEXT((#10176,#10175,#10174))
REPRESENTATION_CONTEXT('MAS-674','TOP_LEVEL_ASSEMBLY_PART')
);
#10149=(
GEOMETRIC_REPRESENTATION_CONTEXT(3)
GLOBAL_UNCERTAINTY_ASSIGNED_CONTEXT((#10165))
GLOBAL_UNIT_ASSIGNED_CONTEXT((#10176,#10175,#10174))
REPRESENTATION_CONTEXT('Part 1','COMPONENT_PART')
);
#10158=UNCERTAINTY_MEASURE_WITH_UNIT(LENGTH_MEASURE(1.E-8),#10176,
'DISTANCE_ACCURACY_VALUE','Maximum Tolerance applied to model');
#10165=UNCERTAINTY_MEASURE_WITH_UNIT(LENGTH_MEASURE(1.E-8),#10176,
'DISTANCE_ACCURACY_VALUE','Maximum Tolerance applied to model');
#10174=(
NAMED_UNIT(*)
SI_UNIT($,.STERADIAN.)
SOLID_ANGLE_UNIT()
);
#10175=(
NAMED_UNIT(*)
PLANE_ANGLE_UNIT()
SI_UNIT($,.RADIAN.)
);
#10176=(
LENGTH_UNIT()
NAMED_UNIT(*)
SI_UNIT($,.METRE.)
);
#10192=PRODUCT_DEFINITION_SHAPE('','',#10217);
#10217=PRODUCT_DEFINITION('','',#10249,#10233);
#10233=PRODUCT_DEFINITION_CONTEXT('',#10323,'design');
#10249=PRODUCT_DEFINITION_FORMATION_WITH_SPECIFIED_SOURCE('','',#10281,
 .NOT_KNOWN.);
#10281=PRODUCT('Part 1','Part 1','Part 1',(#10313));
#10313=PRODUCT_CONTEXT('',#10323,'mechanical');
#10323=APPLICATION_CONTEXT('managed model based 3d engineering');
ENDSEC;
END-ISO-10303-21;
